ISO-10303-21;
HEADER;
FILE_DESCRIPTION (('STEP AP203'),
    '1' );
FILE_NAME ('1602p_c_42.step',
    '2026-10-31T14:11:27',
    ( '' ),
    ( '' ),
    'SwSTEP 2.0',
    'SolidWorks 2024',
    '' );
FILE_SCHEMA (( 'AUTOMOTIVE_DESIGN' ));
ENDSEC;

DATA;
#55=TOROIDAL_SURFACE ( 'NONE', #1961, 3.750000000000000000, 0.5000000000000000000 ) ;
#70=VECTOR ( 'NONE', #6316, 1000.000000000000114 ) ;
#140=( BOUNDED_CURVE ( )  B_SPLINE_CURVE ( 2, ( #4073, #2529, #968 ),
 .UNSPECIFIED., .F., .F. ) 
 B_SPLINE_CURVE_WITH_KNOTS ( ( 3, 3 ),
 ( 0.000000000000000000, 0.2336872276155859962 ),
 .UNSPECIFIED. ) 
 CURVE ( )  GEOMETRIC_REPRESENTATION_ITEM ( )  RATIONAL_B_SPLINE_CURVE ( ( 1.000000000000000000, 1.154700538379259900, 1.000000000000000000 ) ) 
 REPRESENTATION_ITEM ( '' )  );
#143=AXIS2_PLACEMENT_3D ( 'NONE', #12273, #14149, #12491 ) ;
#158=EDGE_CURVE ( 'NONE', #20720, #6814, #11078, .T. ) ;
#228=EDGE_LOOP ( 'NONE', ( #11075, #14429 ) ) ;
#234=CARTESIAN_POINT ( 'NONE',  ( 30.76933207471820708, -4.221800468112564708, -14.00000000000040146 ) ) ;
#252=VERTEX_POINT ( 'NONE', #19862 ) ;
#278=CARTESIAN_POINT ( 'NONE',  ( 28.41185834866789861, -1.882976958576189963, -13.00000000000039968 ) ) ;
#310=EDGE_CURVE ( 'NONE', #20720, #14320, #1201, .T. ) ;
#343=DIRECTION ( 'NONE',  ( -0.9730401042858036753, 0.2306359803922031493, 5.432877459303543355E-17 ) ) ;
#364=DIRECTION ( 'NONE',  ( 0.000000000000000000, 0.000000000000000000, 1.000000000000000000 ) ) ;
#379=CARTESIAN_POINT ( 'NONE',  ( 32.14184541509679605, -2.767081550079640184, -13.00000000000039968 ) ) ;
#415=DIRECTION ( 'NONE',  ( 1.000000000000000000, 0.000000000000000000, 0.000000000000000000 ) ) ;
#420=ORIENTED_EDGE ( 'NONE', *, *, #158, .F. ) ;
#468=AXIS2_PLACEMENT_3D ( 'NONE', #6607, #22852, #3255 ) ;
#507=ORIENTED_EDGE ( 'NONE', *, *, #19720, .T. ) ;
#510=LINE ( 'NONE', #10617, #19480 ) ;
#522=DIRECTION ( 'NONE',  ( 0.000000000000000000, 1.734723475976806848E-16, 1.000000000000000000 ) ) ;
#613=CARTESIAN_POINT ( 'NONE',  ( 31.01827548281339020, -2.500766059351137827, -15.00000000000039613 ) ) ;
#623=( BOUNDED_CURVE ( )  B_SPLINE_CURVE ( 2, ( #18921, #2420, #613 ),
 .UNSPECIFIED., .F., .F. ) 
 B_SPLINE_CURVE_WITH_KNOTS ( ( 3, 3 ),
 ( 0.000000000000000000, 0.1168436138077930952 ),
 .UNSPECIFIED. ) 
 CURVE ( )  GEOMETRIC_REPRESENTATION_ITEM ( )  RATIONAL_B_SPLINE_CURVE ( ( 1.000000000000000000, 1.077350269189630172, 1.077350269189629950 ) ) 
 REPRESENTATION_ITEM ( '' )  );
#630=AXIS2_PLACEMENT_3D ( 'NONE', #10750, #19876, #18085 ) ;
#665=ORIENTED_EDGE ( 'NONE', *, *, #2304, .F. ) ;
#704=DIRECTION ( 'NONE',  ( 0.000000000000000000, 1.020425574104004122E-16, 1.000000000000000000 ) ) ;
#756=( BOUNDED_CURVE ( )  B_SPLINE_CURVE ( 2, ( #16512, #234, #2624 ),
 .UNSPECIFIED., .F., .F. ) 
 B_SPLINE_CURVE_WITH_KNOTS ( ( 3, 3 ),
 ( 0.000000000000000000, 0.2336872276155859962 ),
 .UNSPECIFIED. ) 
 CURVE ( )  GEOMETRIC_REPRESENTATION_ITEM ( )  RATIONAL_B_SPLINE_CURVE ( ( 1.000000000000000000, 1.154700538379259900, 1.000000000000000000 ) ) 
 REPRESENTATION_ITEM ( '' )  );
#811=FACE_OUTER_BOUND ( 'NONE', #5010, .T. ) ;
#878=AXIS2_PLACEMENT_3D ( 'NONE', #4658, #15014, #6561 ) ;
#912=ORIENTED_EDGE ( 'NONE', *, *, #11481, .F. ) ;
#934=DIRECTION ( 'NONE',  ( 0.000000000000000000, 1.020425574104004122E-16, 1.000000000000000000 ) ) ;
#957=LINE ( 'NONE', #10246, #10551 ) ;
#960=LINE ( 'NONE', #12148, #70 ) ;
#968=CARTESIAN_POINT ( 'NONE',  ( 31.37708959083939675, -0.2124270449898580104, -13.00000000000039968 ) ) ;
#977=EDGE_CURVE ( 'NONE', #20686, #18898, #22608, .T. ) ;
#1009=AXIS2_PLACEMENT_3D ( 'NONE', #11223, #5852, #364 ) ;
#1016=AXIS2_PLACEMENT_3D ( 'NONE', #4998, #12267, #10483 ) ;
#1077=EDGE_LOOP ( 'NONE', ( #8086, #17726, #7326, #4054 ) ) ;
#1107=SHAPE_REPRESENTATION ( '1602p_c_42', ( #12739 ), #11790 ) ;
#1123=PLANE ( 'NONE',  #20252 ) ;
#1201=LINE ( 'NONE', #12734, #15743 ) ;
#1204=CARTESIAN_POINT ( 'NONE',  ( 31.11077410011089839, -1.335996977273280262, -15.00000000000039968 ) ) ;
#1216=DIRECTION ( 'NONE',  ( 0.000000000000000000, 0.000000000000000000, 1.000000000000000000 ) ) ;
#1219=CARTESIAN_POINT ( 'NONE',  ( 52.73786095581300515, -7.648876468381259564, -14.25000000000040146 ) ) ;
#1292=CARTESIAN_POINT ( 'NONE',  ( 33.27705887009690144, -3.036156860537199798, -16.37500000000039790 ) ) ;
#1311=MANIFOLD_SOLID_BREP ( 'Imported1', #20140 ) ;
#1328=DIRECTION ( 'NONE',  ( 0.9730401042858036753, -0.2306359803922028995, -5.959266323858677443E-17 ) ) ;
#1376=CARTESIAN_POINT ( 'NONE',  ( 43.98050001724070057, -5.573152644851429471, -13.00000000000039968 ) ) ;
#1384=EDGE_CURVE ( 'NONE', #7111, #12704, #14711, .T. ) ;
#1419=MECHANICAL_CONTEXT ( 'NONE', #2602, 'mechanical' ) ;
#1434=EDGE_LOOP ( 'NONE', ( #6714, #2606, #5028, #4099, #21342 ) ) ;
#1435=EDGE_LOOP ( 'NONE', ( #8667, #19406, #11304, #9513, #2584, #18785 ) ) ;
#1489=CYLINDRICAL_SURFACE ( 'NONE', #9583, 4.250000000000000000 ) ;
#1515=AXIS2_PLACEMENT_3D ( 'NONE', #10906, #1842, #16448 ) ;
#1521=VECTOR ( 'NONE', #2978, 999.9999999999998863 ) ;
#1533=ORIENTED_EDGE ( 'NONE', *, *, #10404, .T. ) ;
#1591=PRODUCT_DEFINITION ( 'UNKNOWN', '', #7231, #1832 ) ;
#1742=CARTESIAN_POINT ( 'NONE',  ( 28.89837840081079889, -1.998294948772289858, -13.00000000000039968 ) ) ;
#1770=DIRECTION ( 'NONE',  ( 0.000000000000000000, 0.000000000000000000, -1.000000000000000000 ) ) ;
#1793=AXIS2_PLACEMENT_3D ( 'NONE', #4710, #10539, #2816 ) ;
#1832=DESIGN_CONTEXT ( 'detailed design', #5484, 'design' ) ;
#1836=DIRECTION ( 'NONE',  ( -0.9730401042858036753, 0.2306359803922028995, 5.959266323858677443E-17 ) ) ;
#1837=EDGE_CURVE ( 'NONE', #18371, #8755, #756, .T. ) ;
#1842=DIRECTION ( 'NONE',  ( -0.1997366180463769070, -0.8426774492125652660, 0.5000000000000002220 ) ) ;
#1860=DIRECTION ( 'NONE',  ( -0.2306359803922028995, -0.9730401042858035643, -1.064172857958375654E-32 ) ) ;
#1905=PLANE ( 'NONE',  #10893 ) ;
#1961=AXIS2_PLACEMENT_3D ( 'NONE', #6347, #16468, #1860 ) ;
#2000=DIRECTION ( 'NONE',  ( -0.2306359803922028717, -0.9730401042858034533, -4.546664459266603656E-32 ) ) ;
#2019=DIRECTION ( 'NONE',  ( 0.000000000000000000, 0.5102823824563427202, -0.8600069128528436968 ) ) ;
#2110=DIRECTION ( 'NONE',  ( 0.000000000000000000, 1.668003342285391304E-16, 1.000000000000000000 ) ) ;
#2190=CYLINDRICAL_SURFACE ( 'NONE', #878, 4.250000000000000000 ) ;
#2191=LINE ( 'NONE', #18478, #22833 ) ;
#2193=CIRCLE ( 'NONE', #10568, 2.500000000000000444 ) ;
#2212=EDGE_LOOP ( 'NONE', ( #20429, #20832, #3918, #6569 ) ) ;
#2244=DIRECTION ( 'NONE',  ( 1.000000000000000000, -8.896220237034308570E-17, 0.000000000000000000 ) ) ;
#2304=EDGE_CURVE ( 'NONE', #16923, #18417, #15003, .T. ) ;
#2342=ORIENTED_EDGE ( 'NONE', *, *, #977, .T. ) ;
#2359=AXIS2_PLACEMENT_3D ( 'NONE', #21399, #12621, #2110 ) ;
#2373=PLANE ( 'NONE',  #9623 ) ;
#2420=CARTESIAN_POINT ( 'NONE',  ( 31.14187293219668362, -1.979315439058181747, -15.00000000000039257 ) ) ;
#2448=DIRECTION ( 'NONE',  ( 1.000000000000000000, 0.000000000000000000, 0.000000000000000000 ) ) ;
#2483=LINE ( 'NONE', #20523, #3980 ) ;
#2529=CARTESIAN_POINT ( 'NONE',  ( 31.56827854690370927, -0.8510906712623020898, -12.00000000000039968 ) ) ;
#2556=CARTESIAN_POINT ( 'NONE',  ( 31.01827548281339020, -2.500766059351137827, -15.00000000000039613 ) ) ;
#2569=CARTESIAN_POINT ( 'NONE',  ( 0.000000000000000000, 0.000000000000000000, 0.000000000000000000 ) ) ;
#2584=ORIENTED_EDGE ( 'NONE', *, *, #5694, .T. ) ;
#2602=APPLICATION_CONTEXT ( 'configuration controlled 3d designs of mechanical parts and assemblies' ) ;
#2606=ORIENTED_EDGE ( 'NONE', *, *, #14710, .T. ) ;
#2624=CARTESIAN_POINT ( 'NONE',  ( 30.31182762792540331, -4.706706774123539994, -13.00000000000039968 ) ) ;
#2641=VERTEX_POINT ( 'NONE', #10053 ) ;
#2815=EDGE_LOOP ( 'NONE', ( #21014, #18100, #1533, #9477, #3921, #13748 ) ) ;
#2816=DIRECTION ( 'NONE',  ( 0.000000000000000000, 0.000000000000000000, -1.000000000000000000 ) ) ;
#2821=ADVANCED_FACE ( 'NONE', ( #3006 ), #17505, .T. ) ;
#2842=CARTESIAN_POINT ( 'NONE',  ( 28.94448933012489888, 0.3641629059906499877, -13.00000000000039968 ) ) ;
#2851=VERTEX_POINT ( 'NONE', #5498 ) ;
#2858=VECTOR ( 'NONE', #1328, 999.9999999999998863 ) ;
#2948=DIRECTION ( 'NONE',  ( -8.623081276789554834E-17, -1.054188326053478339E-16, -1.000000000000000000 ) ) ;
#2978=DIRECTION ( 'NONE',  ( 0.9730401042858036753, -0.2306359803922028995, -5.432877459303547669E-17 ) ) ;
#3005=DIRECTION ( 'NONE',  ( -0.9730401042858035643, 0.2306359803922028717, 5.959266323858677443E-17 ) ) ;
#3006=FACE_OUTER_BOUND ( 'NONE', #228, .T. ) ;
#3039=CARTESIAN_POINT ( 'NONE',  ( 31.14187293219668717, -1.979315439058177528, -11.00000000000039613 ) ) ;
#3075=DIRECTION ( 'NONE',  ( -0.9730401042858036753, 0.2306359803922031493, 5.432877459303543355E-17 ) ) ;
#3106=ADVANCED_FACE ( 'NONE', ( #22543 ), #23003, .T. ) ;
#3171=EDGE_CURVE ( 'NONE', #4894, #8501, #4853, .T. ) ;
#3177=CIRCLE ( 'NONE', #16432, 4.250000000000000000 ) ;
#3180=DIRECTION ( 'NONE',  ( 0.9730401042858035643, -0.2306359803922028717, -5.432877459303547053E-17 ) ) ;
#3255=DIRECTION ( 'NONE',  ( -0.9286452767786568252, -1.871119812896369614E-17, -0.3709689338970204586 ) ) ;
#3267=ADVANCED_FACE ( 'NONE', ( #7691 ), #21815, .F. ) ;
#3309=ORIENTED_EDGE ( 'NONE', *, *, #22532, .F. ) ;
#3319=CONICAL_SURFACE ( 'NONE', #1793, 1.154700538379250796, 1.047197551196598297 ) ;
#3342=ORIENTED_EDGE ( 'NONE', *, *, #9799, .T. ) ;
#3476=DIRECTION ( 'NONE',  ( 0.000000000000000000, 1.734723475976806848E-16, 1.000000000000000000 ) ) ;
#3523=CARTESIAN_POINT ( 'NONE',  ( 30.84445860938240003, -2.459566909556700320, -13.00000000000039968 ) ) ;
#3559=CARTESIAN_POINT ( 'NONE',  ( 33.37436288052550282, -3.059220458576419777, -13.00000000000039968 ) ) ;
#3588=DIRECTION ( 'NONE',  ( -0.9730401042858036753, 0.2306359803922028995, 5.959266323858677443E-17 ) ) ;
#3622=EDGE_CURVE ( 'NONE', #18417, #16923, #23201, .T. ) ;
#3624=CARTESIAN_POINT ( 'NONE',  ( 29.09552749756809931, -4.418411798633290033, -13.00000000000039968 ) ) ;
#3625=DIRECTION ( 'NONE',  ( 0.9730401042858035643, -0.2306359803922028717, -5.432877459303547053E-17 ) ) ;
#3692=CARTESIAN_POINT ( 'NONE',  ( 31.49315201223960159, -2.613324229818170252, -11.84529946162114911 ) ) ;
#3709=CARTESIAN_POINT ( 'NONE',  ( 52.73786095581300515, -7.648876468381259564, -13.00000000000039968 ) ) ;
#3783=CARTESIAN_POINT ( 'NONE',  ( 28.14554285793940025, -3.006546890859610244, -15.00000000000039968 ) ) ;
#3819=DIRECTION ( 'NONE',  ( -9.594916218540590128E-33, 2.583840697242805182E-16, -1.000000000000000000 ) ) ;
#3883=EDGE_CURVE ( 'NONE', #21302, #20737, #2191, .T. ) ;
#3918=ORIENTED_EDGE ( 'NONE', *, *, #3171, .F. ) ;
#3921=ORIENTED_EDGE ( 'NONE', *, *, #1384, .T. ) ;
#3980=VECTOR ( 'NONE', #18526, 999.9999999999998863 ) ;
#4008=ORIENTED_EDGE ( 'NONE', *, *, #11481, .T. ) ;
#4054=ORIENTED_EDGE ( 'NONE', *, *, #14710, .F. ) ;
#4073=CARTESIAN_POINT ( 'NONE',  ( 31.11077410011089839, -1.335996977273280262, -11.00000000000039968 ) ) ;
#4081=DIRECTION ( 'NONE',  ( 0.000000000000000000, 1.668003342285391304E-16, 1.000000000000000000 ) ) ;
#4099=ORIENTED_EDGE ( 'NONE', *, *, #6330, .F. ) ;
#4179=EDGE_CURVE ( 'NONE', #23086, #16983, #19830, .T. ) ;
#4245=ORIENTED_EDGE ( 'NONE', *, *, #13068, .T. ) ;
#4251=ORIENTED_EDGE ( 'NONE', *, *, #5487, .F. ) ;
#4253=CARTESIAN_POINT ( 'NONE',  ( 31.37708959083939675, -0.2124270449898580104, -13.00000000000039968 ) ) ;
#4263=CIRCLE ( 'NONE', #2359, 2.600000000000000089 ) ;
#4457=DIRECTION ( 'NONE',  ( 5.798605125234323991E-17, -1.374421231021384554E-17, 1.000000000000000000 ) ) ;
#4499=DIRECTION ( 'NONE',  ( 0.000000000000000000, 0.000000000000000000, 1.000000000000000000 ) ) ;
#4504=CIRCLE ( 'NONE', #9829, 4.250000000000000000 ) ;
#4529=CARTESIAN_POINT ( 'NONE',  ( 30.89467803343007901, -3.022216679644092796, -11.00000000000039257 ) ) ;
#4613=EDGE_CURVE ( 'NONE', #15338, #18898, #19499, .T. ) ;
#4658=CARTESIAN_POINT ( 'NONE',  ( 30.84445860938240003, -2.459566909556700320, -13.00000000000039968 ) ) ;
#4710=CARTESIAN_POINT ( 'NONE',  ( 31.49315201223960159, -2.613324229818170252, -13.00000000000039968 ) ) ;
#4853=LINE ( 'NONE', #23117, #12788 ) ;
#4876=( NAMED_UNIT ( * ) SI_UNIT ( $, .STERADIAN. ) SOLID_ANGLE_UNIT ( ) );
#4894=VERTEX_POINT ( 'NONE', #21737 ) ;
#4895=ORIENTED_EDGE ( 'NONE', *, *, #14177, .T. ) ;
#4946=CARTESIAN_POINT ( 'NONE',  ( 52.26033179423370001, -7.535689554643980159, -13.00000000000039968 ) ) ;
#4998=CARTESIAN_POINT ( 'NONE',  ( 28.41185834866789861, -1.882976958576189963, -13.00000000000039968 ) ) ;
#5007=CIRCLE ( 'NONE', #22061, 2.009239999999998805 ) ;
#5010=EDGE_LOOP ( 'NONE', ( #4008, #15017 ) ) ;
#5028=ORIENTED_EDGE ( 'NONE', *, *, #14601, .F. ) ;
#5053=EDGE_CURVE ( 'NONE', #19134, #2851, #12529, .T. ) ;
#5114=( LENGTH_UNIT ( ) NAMED_UNIT ( * ) SI_UNIT ( .MILLI., .METRE. ) );
#5182=ORIENTED_EDGE ( 'NONE', *, *, #18231, .F. ) ;
#5205=ORIENTED_EDGE ( 'NONE', *, *, #15038, .T. ) ;
#5257=DIRECTION ( 'NONE',  ( -0.9730401042858035643, 0.2306359803922028717, 5.959266323858677443E-17 ) ) ;
#5282=ORIENTED_EDGE ( 'NONE', *, *, #17214, .T. ) ;
#5365=ADVANCED_FACE ( 'NONE', ( #12783 ), #20262, .F. ) ;
#5386=CARTESIAN_POINT ( 'NONE',  ( 31.11077410011089839, -1.335996977273280262, -11.00000000000039968 ) ) ;
#5441=CARTESIAN_POINT ( 'NONE',  ( 28.67817383939640052, -0.7594070262927730131, -15.00000000000039968 ) ) ;
#5447=CARTESIAN_POINT ( 'NONE',  ( 33.27705887009690144, -3.036156860537205127, -17.25000000000040146 ) ) ;
#5470=EDGE_CURVE ( 'NONE', #14320, #18371, #7307, .T. ) ;
#5484=APPLICATION_CONTEXT ( 'configuration controlled 3d designs of mechanical parts and assemblies' ) ;
#5487=EDGE_CURVE ( 'NONE', #17995, #15230, #7555, .T. ) ;
#5498=CARTESIAN_POINT ( 'NONE',  ( 33.95095283150600807, -0.6266201978619101443, -13.00000000000039968 ) ) ;
#5571=VERTEX_POINT ( 'NONE', #16920 ) ;
#5694=EDGE_CURVE ( 'NONE', #20737, #4894, #17640, .T. ) ;
#5703=CARTESIAN_POINT ( 'NONE',  ( 28.67817383939640052, -0.7594070262927701265, -11.00000000000039968 ) ) ;
#5852=DIRECTION ( 'NONE',  ( -0.9730401042858035643, 0.2306359803922028717, 5.667427308550587516E-17 ) ) ;
#5899=EDGE_CURVE ( 'NONE', #2851, #13535, #19333, .T. ) ;
#5910=EDGE_LOOP ( 'NONE', ( #3309, #20582 ) ) ;
#5949=CIRCLE ( 'NONE', #630, 0.5000000000000004441 ) ;
#6070=EDGE_CURVE ( 'NONE', #20686, #7111, #140, .T. ) ;
#6126=EDGE_CURVE ( 'NONE', #19134, #18417, #13463, .T. ) ;
#6179=DIRECTION ( 'NONE',  ( 0.000000000000000000, 1.734723475976806848E-16, 1.000000000000000000 ) ) ;
#6202=CARTESIAN_POINT ( 'NONE',  ( 52.73786095581300515, -7.648876468381270222, -10.99076000000044928 ) ) ;
#6316=DIRECTION ( 'NONE',  ( 0.1153179901961009640, 0.4865200521429018377, 0.8660254037844385966 ) ) ;
#6330=EDGE_CURVE ( 'NONE', #18371, #8501, #6691, .T. ) ;
#6347=CARTESIAN_POINT ( 'NONE',  ( 28.89837840081079889, -1.998294948772289858, -13.00000000000039968 ) ) ;
#6398=CARTESIAN_POINT ( 'NONE',  ( 32.67740532107718820, -5.566061131680290153, -13.00000000000039968 ) ) ;
#6460=DIRECTION ( 'NONE',  ( 0.9730401042858036753, -0.2306359803922031493, -5.432877459303553216E-17 ) ) ;
#6561=DIRECTION ( 'NONE',  ( 0.000000000000000000, 0.000000000000000000, -1.000000000000000000 ) ) ;
#6569=ORIENTED_EDGE ( 'NONE', *, *, #13866, .F. ) ;
#6607=CARTESIAN_POINT ( 'NONE',  ( 28.94448933012489888, 0.3641629059906499877, -13.00000000000039968 ) ) ;
#6628=EDGE_CURVE ( 'NONE', #18216, #21775, #3177, .T. ) ;
#6642=PRODUCT_DEFINITION_SHAPE ( 'NONE', 'NONE',  #1591 ) ;
#6652=DIRECTION ( 'NONE',  ( 0.1153179901961009640, 0.4865200521429018377, -0.8660254037844385966 ) ) ;
#6659=EDGE_LOOP ( 'NONE', ( #5205, #12488, #21879, #8966, #12043 ) ) ;
#6671=( NAMED_UNIT ( * ) PLANE_ANGLE_UNIT ( ) SI_UNIT ( $, .RADIAN. ) );
#6678=DIRECTION ( 'NONE',  ( -0.9730401042858036753, 0.2306359803922028995, 5.959266323858677443E-17 ) ) ;
#6691=LINE ( 'NONE', #13924, #22069 ) ;
#6714=ORIENTED_EDGE ( 'NONE', *, *, #19359, .F. ) ;
#6733=DIRECTION ( 'NONE',  ( -0.9730401042858035643, 0.2306359803922028717, 5.959266323858679908E-17 ) ) ;
#6750=ORIENTED_EDGE ( 'NONE', *, *, #16840, .T. ) ;
#6771=CARTESIAN_POINT ( 'NONE',  ( 32.79777292954499757, -5.491820719290930519, -13.00000000000039968 ) ) ;
#6790=LINE ( 'NONE', #12030, #1521 ) ;
#6796=FACE_OUTER_BOUND ( 'NONE', #13869, .T. ) ;
#6814=VERTEX_POINT ( 'NONE', #8316 ) ;
#6891=ADVANCED_FACE ( 'NONE', ( #21587 ), #17175, .F. ) ;
#6981=ORIENTED_EDGE ( 'NONE', *, *, #10859, .F. ) ;
#6997=EDGE_LOOP ( 'NONE', ( #20371, #18432, #12071, #13074, #7451 ) ) ;
#7111=VERTEX_POINT ( 'NONE', #4253 ) ;
#7123=LINE ( 'NONE', #8664, #16425 ) ;
#7201=DIRECTION ( 'NONE',  ( 0.000000000000000000, 1.156482317317871478E-16, 1.000000000000000000 ) ) ;
#7224=EDGE_LOOP ( 'NONE', ( #14371, #17481, #12620, #17671, #14966 ) ) ;
#7230=ORIENTED_EDGE ( 'NONE', *, *, #17042, .F. ) ;
#7231=PRODUCT_DEFINITION_FORMATION_WITH_SPECIFIED_SOURCE ( 'ANY', '', #15912, .NOT_KNOWN. ) ;
#7233=CARTESIAN_POINT ( 'NONE',  ( 52.49909637502329929, -7.592283011512620305, -15.25462000000040064 ) ) ;
#7265=EDGE_LOOP ( 'NONE', ( #22520, #5282, #12354, #6750, #4245 ) ) ;
#7279=ORIENTED_EDGE ( 'NONE', *, *, #6628, .F. ) ;
#7298=CARTESIAN_POINT ( 'NONE',  ( 28.89837840081079889, -1.998294948772289858, -13.00000000000039968 ) ) ;
#7307=( BOUNDED_CURVE ( )  B_SPLINE_CURVE ( 2, ( #2556, #11836, #10060 ),
 .UNSPECIFIED., .F., .F. ) 
 B_SPLINE_CURVE_WITH_KNOTS ( ( 3, 3 ),
 ( 0.1168436138077930952, 0.2336872276155859962 ),
 .UNSPECIFIED. ) 
 CURVE ( )  GEOMETRIC_REPRESENTATION_ITEM ( )  RATIONAL_B_SPLINE_CURVE ( ( 1.077350269189629950, 1.077350269189629728, 1.000000000000000000 ) ) 
 REPRESENTATION_ITEM ( '' )  );
#7315=DIRECTION ( 'NONE',  ( 0.000000000000000000, 0.000000000000000000, 1.000000000000000000 ) ) ;
#7326=ORIENTED_EDGE ( 'NONE', *, *, #16363, .F. ) ;
#7423=CARTESIAN_POINT ( 'NONE',  ( 33.27705887009690144, -3.036156860537199798, -13.00000000000039968 ) ) ;
#7448=VERTEX_POINT ( 'NONE', #19895 ) ;
#7451=ORIENTED_EDGE ( 'NONE', *, *, #10404, .F. ) ;
#7517=ORIENTED_EDGE ( 'NONE', *, *, #1837, .T. ) ;
#7555=CIRCLE ( 'NONE', #11420, 0.1000000000000028644 ) ;
#7592=EDGE_LOOP ( 'NONE', ( #11467, #18977, #912, #20480, #16499 ) ) ;
#7622=CARTESIAN_POINT ( 'NONE',  ( 28.54501609403209983, -1.321191992434479934, -15.00000000000039968 ) ) ;
#7691=FACE_OUTER_BOUND ( 'NONE', #1434, .T. ) ;
#7693=AXIS2_PLACEMENT_3D ( 'NONE', #10516, #6460, #21179 ) ;
#7698=ORIENTED_EDGE ( 'NONE', *, *, #2304, .T. ) ;
#7712=SHAPE_REPRESENTATION_RELATIONSHIP ( 'NONE' , 'NONE' ,  #1107, #12489 ) ;
#7719=CIRCLE ( 'NONE', #13035, 3.750000000000000000 ) ;
#8070=VECTOR ( 'NONE', #21154, 1000.000000000000114 ) ;
#8078=CIRCLE ( 'NONE', #16033, 0.5000000000000000000 ) ;
#8086=ORIENTED_EDGE ( 'NONE', *, *, #1384, .F. ) ;
#8136=ADVANCED_FACE ( 'NONE', ( #11541 ), #18775, .T. ) ;
#8208=EDGE_CURVE ( 'NONE', #14326, #2641, #8078, .T. ) ;
#8218=CARTESIAN_POINT ( 'NONE',  ( 31.01827548281339375, -2.500766059351137827, -11.00000000000039435 ) ) ;
#8250=CARTESIAN_POINT ( 'NONE',  ( 30.76933207471821774, -4.221800468112557603, -12.00000000000039968 ) ) ;
#8264=CIRCLE ( 'NONE', #20760, 2.600000000000000089 ) ;
#8316=CARTESIAN_POINT ( 'NONE',  ( 31.01827548281339375, -2.500766059351137827, -11.00000000000039435 ) ) ;
#8341=ORIENTED_EDGE ( 'NONE', *, *, #310, .T. ) ;
#8453=ORIENTED_EDGE ( 'NONE', *, *, #5053, .F. ) ;
#8476=DIRECTION ( 'NONE',  ( -0.6880432561069586006, 0.1630842657209346236, 0.7071067811865459074 ) ) ;
#8480=AXIS2_PLACEMENT_3D ( 'NONE', #17446, #3075, #934 ) ;
#8492=DIRECTION ( 'NONE',  ( 0.9730401042858035643, -0.2306359803922028717, -5.959266323858674978E-17 ) ) ;
#8495=CARTESIAN_POINT ( 'NONE',  ( 30.31182762792540331, -4.706706774123539994, -13.00000000000039968 ) ) ;
#8501=VERTEX_POINT ( 'NONE', #18029 ) ;
#8645=DIRECTION ( 'NONE',  ( 0.000000000000000000, 0.000000000000000000, -1.000000000000000000 ) ) ;
#8664=CARTESIAN_POINT ( 'NONE',  ( 43.98050001724070057, -5.573152644851429471, -15.50000000000040146 ) ) ;
#8667=ORIENTED_EDGE ( 'NONE', *, *, #14601, .T. ) ;
#8722=DIRECTION ( 'NONE',  ( -0.1153179901961009640, -0.4865200521429018377, -0.8660254037844385966 ) ) ;
#8731=CARTESIAN_POINT ( 'NONE',  ( 30.84445860938240003, -2.459566909556699876, -8.750000000000399680 ) ) ;
#8755=VERTEX_POINT ( 'NONE', #18963 ) ;
#8788=ADVANCED_FACE ( 'NONE', ( #23085, #12207 ), #1123, .T. ) ;
#8792=AXIS2_PLACEMENT_3D ( 'NONE', #3783, #18296, #2019 ) ;
#8841=CARTESIAN_POINT ( 'NONE',  ( 29.27674327513866004, 1.765923432495573264, -13.00000000000039968 ) ) ;
#8861=FACE_OUTER_BOUND ( 'NONE', #2815, .T. ) ;
#8879=DIRECTION ( 'NONE',  ( 0.9730401042858036753, -0.2306359803922031493, -5.959266323858673745E-17 ) ) ;
#8955=UNCERTAINTY_MEASURE_WITH_UNIT (LENGTH_MEASURE( 1.000000000000000082E-05 ), #5114, 'distance_accuracy_value', 'NONE');
#8966=ORIENTED_EDGE ( 'NONE', *, *, #6628, .T. ) ;
#9191=CARTESIAN_POINT ( 'NONE',  ( 28.14554285793940025, -3.006546890859610244, -11.00000000000039968 ) ) ;
#9392=DIRECTION ( 'NONE',  ( -0.9730401042858035643, 0.2306359803922028717, 6.126766849694256332E-17 ) ) ;
#9477=ORIENTED_EDGE ( 'NONE', *, *, #6070, .T. ) ;
#9513=ORIENTED_EDGE ( 'NONE', *, *, #23113, .T. ) ;
#9583=AXIS2_PLACEMENT_3D ( 'NONE', #3523, #19562, #10448 ) ;
#9623=AXIS2_PLACEMENT_3D ( 'NONE', #9756, #16857, #2244 ) ;
#9628=CARTESIAN_POINT ( 'NONE',  ( 33.27705887009690144, -3.036156860537205127, -8.750000000000399680 ) ) ;
#9630=DIRECTION ( 'NONE',  ( 0.9730401042858035643, -0.2306359803922028717, -5.432877459303547053E-17 ) ) ;
#9666=DIRECTION ( 'NONE',  ( 0.2306359803922028995, 0.9730401042858036753, -9.756037151021835575E-16 ) ) ;
#9756=CARTESIAN_POINT ( 'NONE',  ( 28.14554285793940025, -3.006546890859610244, -11.00000000000039968 ) ) ;
#9799=EDGE_CURVE ( 'NONE', #18216, #16983, #6790, .T. ) ;
#9829=AXIS2_PLACEMENT_3D ( 'NONE', #19146, #10126, #21032 ) ;
#9864=DIRECTION ( 'NONE',  ( -9.594916218540590128E-33, 2.583840697242805182E-16, -1.000000000000000000 ) ) ;
#9945=VECTOR ( 'NONE', #16398, 1000.000000000000114 ) ;
#9984=DIRECTION ( 'NONE',  ( 0.000000000000000000, 0.000000000000000000, -1.000000000000000000 ) ) ;
#10053=CARTESIAN_POINT ( 'NONE',  ( 29.87858131747766421, 2.137125494442374318, -13.00000000000039968 ) ) ;
#10060=CARTESIAN_POINT ( 'NONE',  ( 30.57814311865390167, -3.583136841840119935, -15.00000000000039968 ) ) ;
#10121=AXIS2_PLACEMENT_3D ( 'NONE', #1742, #14347, #23471 ) ;
#10126=DIRECTION ( 'NONE',  ( -0.9730401042858036753, 0.2306359803922031493, 5.432877459303543355E-17 ) ) ;
#10199=DIRECTION ( 'NONE',  ( 0.9730401042858035643, -0.2306359803922028717, -5.432877459303547053E-17 ) ) ;
#10246=CARTESIAN_POINT ( 'NONE',  ( 29.89447396975359794, -1.047702001783030079, -15.00000000000039968 ) ) ;
#10310=CARTESIAN_POINT ( 'NONE',  ( 31.11077410011089839, -1.335996977273280262, -11.00000000000039968 ) ) ;
#10319=ORIENTED_EDGE ( 'NONE', *, *, #15038, .F. ) ;
#10376=CARTESIAN_POINT ( 'NONE',  ( 30.57814311865390167, -3.583136841840119935, -11.00000000000039968 ) ) ;
#10404=EDGE_CURVE ( 'NONE', #6814, #20686, #17914, .T. ) ;
#10417=FACE_OUTER_BOUND ( 'NONE', #1077, .T. ) ;
#10431=CARTESIAN_POINT ( 'NONE',  ( 28.41185834866789861, -1.882976958576189963, -16.27970053837969999 ) ) ;
#10448=DIRECTION ( 'NONE',  ( 0.000000000000000000, 0.000000000000000000, -1.000000000000000000 ) ) ;
#10483=DIRECTION ( 'NONE',  ( 0.000000000000000000, 1.156482317317871478E-16, 1.000000000000000000 ) ) ;
#10507=( BOUNDED_CURVE ( )  B_SPLINE_CURVE ( 2, ( #8495, #8250, #21064 ),
 .UNSPECIFIED., .F., .F. ) 
 B_SPLINE_CURVE_WITH_KNOTS ( ( 3, 3 ),
 ( 0.000000000000000000, 0.2336872276155859962 ),
 .UNSPECIFIED. ) 
 CURVE ( )  GEOMETRIC_REPRESENTATION_ITEM ( )  RATIONAL_B_SPLINE_CURVE ( ( 1.000000000000000000, 1.154700538379249908, 1.000000000000000000 ) ) 
 REPRESENTATION_ITEM ( '' )  );
#10516=CARTESIAN_POINT ( 'NONE',  ( 33.27705887009690144, -3.036156860537199798, -13.00000000000039968 ) ) ;
#10533=AXIS2_PLACEMENT_3D ( 'NONE', #16073, #16290, #3476 ) ;
#10539=DIRECTION ( 'NONE',  ( -0.9730401042858035643, 0.2306359803922028717, 5.432877459303547053E-17 ) ) ;
#10542=AXIS2_PLACEMENT_3D ( 'NONE', #18299, #10838, #1770 ) ;
#10551=VECTOR ( 'NONE', #6678, 999.9999999999998863 ) ;
#10568=AXIS2_PLACEMENT_3D ( 'NONE', #20710, #18831, #522 ) ;
#10617=CARTESIAN_POINT ( 'NONE',  ( 52.49909637502329929, -7.592283011512620305, -10.74538000000039872 ) ) ;
#10625=CARTESIAN_POINT ( 'NONE',  ( 31.01827548281339020, -2.500766059351137827, -15.00000000000039435 ) ) ;
#10750=CARTESIAN_POINT ( 'NONE',  ( 28.03349347434003747, -5.647195339844054196, -13.00000000000039968 ) ) ;
#10757=ORIENTED_EDGE ( 'NONE', *, *, #16938, .F. ) ;
#10812=CARTESIAN_POINT ( 'NONE',  ( 28.89837840081079534, -1.998294948772295410, -17.25000000000040146 ) ) ;
#10838=DIRECTION ( 'NONE',  ( 0.9730401042858036753, -0.2306359803922031493, -5.432877459303553216E-17 ) ) ;
#10859=EDGE_CURVE ( 'NONE', #8755, #21302, #10507, .T. ) ;
#10893=AXIS2_PLACEMENT_3D ( 'NONE', #5703, #12505, #11211 ) ;
#10906=CARTESIAN_POINT ( 'NONE',  ( 27.87922736721089834, -4.130116823143030302, -13.00000000000039968 ) ) ;
#10913=AXIS2_PLACEMENT_3D ( 'NONE', #17394, #3005, #1216 ) ;
#11075=ORIENTED_EDGE ( 'NONE', *, *, #14177, .F. ) ;
#11078=LINE ( 'NONE', #3692, #9945 ) ;
#11106=CARTESIAN_POINT ( 'NONE',  ( 33.97401642954523737, -0.5293161874333298655, -13.00000000000039968 ) ) ;
#11108=FACE_OUTER_BOUND ( 'NONE', #6659, .T. ) ;
#11188=CARTESIAN_POINT ( 'NONE',  ( 30.16078946048209630, 0.07586793050039619679, -13.00000000000039968 ) ) ;
#11191=ADVANCED_FACE ( 'NONE', ( #13331 ), #11297, .T. ) ;
#11211=DIRECTION ( 'NONE',  ( 0.9286452767786566032, 1.871119812896368998E-17, -0.3709689338970208472 ) ) ;
#11223=CARTESIAN_POINT ( 'NONE',  ( 52.49909637502329929, -7.592283011512620305, -13.00000000000039968 ) ) ;
#11297=CONICAL_SURFACE ( 'NONE', #1009, 2.254620000000000513, 0.7853981633974461696 ) ;
#11304=ORIENTED_EDGE ( 'NONE', *, *, #4613, .T. ) ;
#11311=FACE_OUTER_BOUND ( 'NONE', #6997, .T. ) ;
#11322=ORIENTED_EDGE ( 'NONE', *, *, #14337, .F. ) ;
#11420=AXIS2_PLACEMENT_3D ( 'NONE', #18602, #4457, #2448 ) ;
#11467=ORIENTED_EDGE ( 'NONE', *, *, #13068, .F. ) ;
#11481=EDGE_CURVE ( 'NONE', #16983, #23086, #20757, .T. ) ;
#11520=CARTESIAN_POINT ( 'NONE',  ( 27.91817548414393713, -6.133715391986954479, -13.00000000000039968 ) ) ;
#11541=FACE_OUTER_BOUND ( 'NONE', #20533, .T. ) ;
#11775=ORIENTED_EDGE ( 'NONE', *, *, #17042, .T. ) ;
#11790=( GEOMETRIC_REPRESENTATION_CONTEXT ( 3 ) GLOBAL_UNCERTAINTY_ASSIGNED_CONTEXT ( ( #8955 ) ) GLOBAL_UNIT_ASSIGNED_CONTEXT ( ( #5114, #6671, #4876 ) ) REPRESENTATION_CONTEXT ( 'NONE', 'WORKASPACE' ) );
#11836=CARTESIAN_POINT ( 'NONE',  ( 30.89467803343009678, -3.022216679644093240, -15.00000000000039968 ) ) ;
#11842=CARTESIAN_POINT ( 'NONE',  ( 29.89447396975359794, -1.047702001783019865, -11.00000000000039968 ) ) ;
#11935=CARTESIAN_POINT ( 'NONE',  ( 28.74475271207850113, -0.4785145432219160000, -11.50000000000039968 ) ) ;
#12030=CARTESIAN_POINT ( 'NONE',  ( 30.84445860938240003, -2.459566909556700320, -17.25000000000040146 ) ) ;
#12043=ORIENTED_EDGE ( 'NONE', *, *, #14333, .F. ) ;
#12071=ORIENTED_EDGE ( 'NONE', *, *, #23113, .F. ) ;
#12096=CARTESIAN_POINT ( 'NONE',  ( 31.01827548281339375, -2.500766059351137827, -11.00000000000039435 ) ) ;
#12148=CARTESIAN_POINT ( 'NONE',  ( 28.87791045744280183, 0.08327042291979450117, -13.50000000000040146 ) ) ;
#12207=FACE_OUTER_BOUND ( 'NONE', #17198, .T. ) ;
#12264=ORIENTED_EDGE ( 'NONE', *, *, #5899, .T. ) ;
#12267=DIRECTION ( 'NONE',  ( 0.9730401042858036753, -0.2306359803922031493, -5.959266323858673745E-17 ) ) ;
#12273=CARTESIAN_POINT ( 'NONE',  ( 33.37436288052550282, -3.059220458576419777, -13.00000000000039968 ) ) ;
#12354=ORIENTED_EDGE ( 'NONE', *, *, #14333, .T. ) ;
#12366=ORIENTED_EDGE ( 'NONE', *, *, #16368, .T. ) ;
#12458=CARTESIAN_POINT ( 'NONE',  ( 29.76326332728156032, 1.650605442299475145, -13.00000000000039968 ) ) ;
#12466=DIRECTION ( 'NONE',  ( -0.6880432561069586006, 0.1630842657209347069, -0.7071067811865459074 ) ) ;
#12488=ORIENTED_EDGE ( 'NONE', *, *, #8208, .T. ) ;
#12489=ADVANCED_BREP_SHAPE_REPRESENTATION ( '', ( #1311, #12739 ), #11790 ) ;
#12491=DIRECTION ( 'NONE',  ( -0.2306359803922028717, -0.9730401042858034533, -4.546664459266603656E-32 ) ) ;
#12505=DIRECTION ( 'NONE',  ( 0.1997366180463769070, 0.8426774492125652660, 0.5000000000000003331 ) ) ;
#12519=DIRECTION ( 'NONE',  ( 0.000000000000000000, 0.000000000000000000, 1.000000000000000000 ) ) ;
#12529=CIRCLE ( 'NONE', #14023, 2.500000000000000444 ) ;
#12558=CYLINDRICAL_SURFACE ( 'NONE', #20936, 2.500000000000000444 ) ;
#12620=ORIENTED_EDGE ( 'NONE', *, *, #18231, .T. ) ;
#12621=DIRECTION ( 'NONE',  ( 0.9730401042858035643, -0.2306359803922028717, -5.959266323858667582E-17 ) ) ;
#12668=LINE ( 'NONE', #3624, #18897 ) ;
#12699=DIRECTION ( 'NONE',  ( 0.000000000000000000, 1.734723475976806848E-16, 1.000000000000000000 ) ) ;
#12704=VERTEX_POINT ( 'NONE', #13474 ) ;
#12717=SHAPE_DEFINITION_REPRESENTATION ( #6642, #1107 ) ;
#12734=CARTESIAN_POINT ( 'NONE',  ( 31.49315201223960159, -2.613324229818170252, -14.15470053837965025 ) ) ;
#12739=AXIS2_PLACEMENT_3D ( 'NONE', #2569, #13380, #415 ) ;
#12783=FACE_OUTER_BOUND ( 'NONE', #16173, .T. ) ;
#12788=VECTOR ( 'NONE', #6652, 1000.000000000000114 ) ;
#12826=FACE_OUTER_BOUND ( 'NONE', #2212, .T. ) ;
#12839=ORIENTED_EDGE ( 'NONE', *, *, #3622, .T. ) ;
#13014=CARTESIAN_POINT ( 'NONE',  ( 52.73786095581300515, -7.648876468381270222, -15.00924000000035008 ) ) ;
#13035=AXIS2_PLACEMENT_3D ( 'NONE', #278, #8879, #7201 ) ;
#13068=EDGE_CURVE ( 'NONE', #5571, #2641, #4504, .T. ) ;
#13074=ORIENTED_EDGE ( 'NONE', *, *, #977, .F. ) ;
#13086=CARTESIAN_POINT ( 'NONE',  ( 28.89837840081079889, -1.998294948772289858, -13.00000000000039968 ) ) ;
#13190=VERTEX_POINT ( 'NONE', #6202 ) ;
#13331=FACE_OUTER_BOUND ( 'NONE', #20260, .T. ) ;
#13380=DIRECTION ( 'NONE',  ( 0.000000000000000000, 0.000000000000000000, 1.000000000000000000 ) ) ;
#13386=CIRCLE ( 'NONE', #8480, 4.250000000000000000 ) ;
#13402=AXIS2_PLACEMENT_3D ( 'NONE', #17079, #9630, #9984 ) ;
#13412=( BOUNDED_CURVE ( )  B_SPLINE_CURVE ( 2, ( #10376, #4529, #8218 ),
 .UNSPECIFIED., .F., .T. ) 
 B_SPLINE_CURVE_WITH_KNOTS ( ( 3, 3 ),
 ( 0.000000000000000000, 0.1168436138077924430 ),
 .UNSPECIFIED. ) 
 CURVE ( )  GEOMETRIC_REPRESENTATION_ITEM ( )  RATIONAL_B_SPLINE_CURVE ( ( 1.000000000000000000, 1.077350269189624621, 1.077350269189625065 ) ) 
 REPRESENTATION_ITEM ( '' )  );
#13463=LINE ( 'NONE', #20695, #14767 ) ;
#13474=CARTESIAN_POINT ( 'NONE',  ( 31.11077410011089839, -1.335996977273280262, -15.00000000000039968 ) ) ;
#13504=ORIENTED_EDGE ( 'NONE', *, *, #16938, .T. ) ;
#13527=DIRECTION ( 'NONE',  ( -0.9730401042858035643, 0.2306359803922028717, 5.667427308550587516E-17 ) ) ;
#13535=VERTEX_POINT ( 'NONE', #16936 ) ;
#13622=ADVANCED_FACE ( 'NONE', ( #17535 ), #3319, .F. ) ;
#13665=VECTOR ( 'NONE', #8722, 1000.000000000000114 ) ;
#13748=ORIENTED_EDGE ( 'NONE', *, *, #19359, .T. ) ;
#13765=ORIENTED_EDGE ( 'NONE', *, *, #15937, .T. ) ;
#13821=CARTESIAN_POINT ( 'NONE',  ( 31.37708959083939675, -0.2124270449898580104, -13.00000000000039968 ) ) ;
#13859=DIRECTION ( 'NONE',  ( 0.000000000000000000, 0.000000000000000000, 1.000000000000000000 ) ) ;
#13866=EDGE_CURVE ( 'NONE', #8755, #4894, #12668, .T. ) ;
#13869=EDGE_LOOP ( 'NONE', ( #17190, #23014, #12264, #507, #4251 ) ) ;
#13924=CARTESIAN_POINT ( 'NONE',  ( 29.36184298829660122, -3.294841866349869974, -15.00000000000039968 ) ) ;
#13925=VECTOR ( 'NONE', #9666, 999.9999999999998863 ) ;
#13965=DIRECTION ( 'NONE',  ( 6.124378941433959925E-17, 0.000000000000000000, 1.000000000000000000 ) ) ;
#13991=EDGE_CURVE ( 'NONE', #2851, #21488, #2193, .T. ) ;
#13998=DIRECTION ( 'NONE',  ( 0.9730401042858035643, -0.2306359803922028717, -5.959266323858674978E-17 ) ) ;
#14023=AXIS2_PLACEMENT_3D ( 'NONE', #18787, #9392, #6179 ) ;
#14149=DIRECTION ( 'NONE',  ( 0.9730401042858035643, -0.2306359803922028717, -5.959266323858677443E-17 ) ) ;
#14177=EDGE_CURVE ( 'NONE', #13190, #17080, #16186, .T. ) ;
#14320=VERTEX_POINT ( 'NONE', #10625 ) ;
#14326=VERTEX_POINT ( 'NONE', #8841 ) ;
#14333=EDGE_CURVE ( 'NONE', #7448, #21775, #5949, .T. ) ;
#14337=EDGE_CURVE ( 'NONE', #17995, #19134, #17330, .T. ) ;
#14347=DIRECTION ( 'NONE',  ( -0.9730401042858036753, 0.2306359803922031493, 5.432877459303543355E-17 ) ) ;
#14358=DIRECTION ( 'NONE',  ( 0.9730401042858035643, -0.2306359803922028717, -5.959266323858677443E-17 ) ) ;
#14371=ORIENTED_EDGE ( 'NONE', *, *, #5899, .F. ) ;
#14429=ORIENTED_EDGE ( 'NONE', *, *, #15937, .F. ) ;
#14468=DIRECTION ( 'NONE',  ( -0.9730401042858035643, 0.2306359803922028717, 6.126766849694256332E-17 ) ) ;
#14541=DIRECTION ( 'NONE',  ( 0.9730401042858035643, -0.2306359803922028717, -5.959266323858677443E-17 ) ) ;
#14542=ORIENTED_EDGE ( 'NONE', *, *, #21001, .F. ) ;
#14570=ORIENTED_EDGE ( 'NONE', *, *, #17214, .F. ) ;
#14601=EDGE_CURVE ( 'NONE', #8501, #252, #22458, .T. ) ;
#14710=EDGE_CURVE ( 'NONE', #12704, #252, #957, .T. ) ;
#14711=( BOUNDED_CURVE ( )  B_SPLINE_CURVE ( 2, ( #13821, #22347, #1204 ),
 .UNSPECIFIED., .F., .F. ) 
 B_SPLINE_CURVE_WITH_KNOTS ( ( 3, 3 ),
 ( 0.000000000000000000, 0.2336872276155859962 ),
 .UNSPECIFIED. ) 
 CURVE ( )  GEOMETRIC_REPRESENTATION_ITEM ( )  RATIONAL_B_SPLINE_CURVE ( ( 1.000000000000000000, 1.154700538379259900, 1.000000000000000000 ) ) 
 REPRESENTATION_ITEM ( '' )  );
#14767=VECTOR ( 'NONE', #20344, 999.9999999999998863 ) ;
#14966=ORIENTED_EDGE ( 'NONE', *, *, #22532, .T. ) ;
#14990=EDGE_LOOP ( 'NONE', ( #420, #8341, #16004, #7517, #17693, #12366 ) ) ;
#15003=CIRCLE ( 'NONE', #23349, 2.500000000000000444 ) ;
#15014=DIRECTION ( 'NONE',  ( 0.9730401042858035643, -0.2306359803922028717, -5.432877459303547053E-17 ) ) ;
#15017=ORIENTED_EDGE ( 'NONE', *, *, #4179, .T. ) ;
#15038=EDGE_CURVE ( 'NONE', #7448, #14326, #18488, .T. ) ;
#15215=ADVANCED_FACE ( 'NONE', ( #12826 ), #20059, .F. ) ;
#15230=VERTEX_POINT ( 'NONE', #6398 ) ;
#15338=VERTEX_POINT ( 'NONE', #2842 ) ;
#15409=ORIENTED_EDGE ( 'NONE', *, *, #13866, .T. ) ;
#15531=AXIS2_PLACEMENT_3D ( 'NONE', #11106, #18460, #18099 ) ;
#15569=ADVANCED_FACE ( 'NONE', ( #18940 ), #55, .T. ) ;
#15673=PLANE ( 'NONE',  #18321 ) ;
#15736=PLANE ( 'NONE',  #468 ) ;
#15743=VECTOR ( 'NONE', #19967, 1000.000000000000000 ) ;
#15786=FACE_BOUND ( 'NONE', #5910, .T. ) ;
#15846=CARTESIAN_POINT ( 'NONE',  ( 27.94580623989299895, -3.849224340072180173, -12.50000000000040146 ) ) ;
#15875=FACE_OUTER_BOUND ( 'NONE', #21683, .T. ) ;
#15883=DIRECTION ( 'NONE',  ( 0.000000000000000000, 1.000000000000000000, 0.000000000000000000 ) ) ;
#15912=PRODUCT ( '1602p_c_42', '1602p_c_42', '', ( #1419 ) ) ;
#15937=EDGE_CURVE ( 'NONE', #17080, #13190, #5007, .T. ) ;
#16004=ORIENTED_EDGE ( 'NONE', *, *, #5470, .T. ) ;
#16012=CARTESIAN_POINT ( 'NONE',  ( 52.26033179423370001, -7.535689554643993482, -15.50000000000040146 ) ) ;
#16033=AXIS2_PLACEMENT_3D ( 'NONE', #12458, #2948, #15883 ) ;
#16073=CARTESIAN_POINT ( 'NONE',  ( 33.37436288052550282, -3.059220458576419777, -13.00000000000039968 ) ) ;
#16173=EDGE_LOOP ( 'NONE', ( #6981, #15409, #19676, #22145 ) ) ;
#16186=CIRCLE ( 'NONE', #10913, 2.009239999999998805 ) ;
#16201=LINE ( 'NONE', #8731, #19628 ) ;
#16202=CONICAL_SURFACE ( 'NONE', #20002, 1.154700538379250796, 1.047197551196598297 ) ;
#16286=ORIENTED_EDGE ( 'NONE', *, *, #4179, .F. ) ;
#16290=DIRECTION ( 'NONE',  ( -0.9730401042858035643, 0.2306359803922028717, 6.126766849694256332E-17 ) ) ;
#16309=DIRECTION ( 'NONE',  ( -0.9730401042858035643, 0.2306359803922028717, 5.432877459303547053E-17 ) ) ;
#16363=EDGE_CURVE ( 'NONE', #252, #15338, #960, .T. ) ;
#16368=EDGE_CURVE ( 'NONE', #21302, #6814, #13412, .T. ) ;
#16372=LINE ( 'NONE', #11188, #2858 ) ;
#16398=DIRECTION ( 'NONE',  ( -0.4865200521429014491, 0.1153179901961012555, 0.8660254037844388186 ) ) ;
#16401=FACE_OUTER_BOUND ( 'NONE', #23449, .T. ) ;
#16425=VECTOR ( 'NONE', #21580, 999.9999999999998863 ) ;
#16432=AXIS2_PLACEMENT_3D ( 'NONE', #13086, #343, #704 ) ;
#16448=DIRECTION ( 'NONE',  ( -0.9730401042858036753, 0.2306359803922023999, -1.110223024625155524E-17 ) ) ;
#16457=TOROIDAL_SURFACE ( 'NONE', #143, 2.600000000000000089, 0.1000000000000000056 ) ;
#16468=DIRECTION ( 'NONE',  ( 0.9730401042858035643, -0.2306359803922028717, -5.959266323858677443E-17 ) ) ;
#16469=DIRECTION ( 'NONE',  ( -2.829953705592110306E-16, -9.355573283744330345E-16, -1.000000000000000000 ) ) ;
#16499=ORIENTED_EDGE ( 'NONE', *, *, #21659, .F. ) ;
#16512=CARTESIAN_POINT ( 'NONE',  ( 30.57814311865390167, -3.583136841840119935, -15.00000000000039968 ) ) ;
#16652=ADVANCED_FACE ( 'NONE', ( #11311 ), #2373, .F. ) ;
#16770=ORIENTED_EDGE ( 'NONE', *, *, #22829, .T. ) ;
#16806=TOROIDAL_SURFACE ( 'NONE', #18731, 3.750000000000000000, 0.5000000000000000000 ) ;
#16811=ADVANCED_FACE ( 'NONE', ( #811, #15786 ), #15673, .T. ) ;
#16840=EDGE_CURVE ( 'NONE', #21775, #5571, #13386, .T. ) ;
#16857=DIRECTION ( 'NONE',  ( 1.040345436475888435E-32, 1.169424102322700040E-16, 1.000000000000000000 ) ) ;
#16920=CARTESIAN_POINT ( 'NONE',  ( 28.89837840081079889, -1.998294948772295410, -8.750000000000399680 ) ) ;
#16923=VERTEX_POINT ( 'NONE', #16012 ) ;
#16936=CARTESIAN_POINT ( 'NONE',  ( 33.87671241911665021, -0.5062525893941096644, -13.00000000000039968 ) ) ;
#16938=EDGE_CURVE ( 'NONE', #17080, #16923, #19696, .T. ) ;
#16983=VERTEX_POINT ( 'NONE', #5447 ) ;
#17042=EDGE_CURVE ( 'NONE', #21488, #16923, #7123, .T. ) ;
#17079=CARTESIAN_POINT ( 'NONE',  ( 43.98050001724070057, -5.573152644851429471, -13.00000000000039968 ) ) ;
#17080=VERTEX_POINT ( 'NONE', #13014 ) ;
#17175=TOROIDAL_SURFACE ( 'NONE', #20213, 2.600000000000000089, 0.1000000000000000056 ) ;
#17190=ORIENTED_EDGE ( 'NONE', *, *, #14337, .T. ) ;
#17198=EDGE_LOOP ( 'NONE', ( #10319, #14570 ) ) ;
#17214=EDGE_CURVE ( 'NONE', #14326, #7448, #7719, .T. ) ;
#17320=AXIS2_PLACEMENT_3D ( 'NONE', #1219, #8492, #3819 ) ;
#17330=CIRCLE ( 'NONE', #10533, 2.500000000000000444 ) ;
#17388=ADVANCED_FACE ( 'NONE', ( #20606 ), #2190, .T. ) ;
#17394=CARTESIAN_POINT ( 'NONE',  ( 52.73786095581300515, -7.648876468381259564, -13.00000000000039968 ) ) ;
#17430=ORIENTED_EDGE ( 'NONE', *, *, #4613, .F. ) ;
#17446=CARTESIAN_POINT ( 'NONE',  ( 28.89837840081079889, -1.998294948772289858, -13.00000000000039968 ) ) ;
#17481=ORIENTED_EDGE ( 'NONE', *, *, #13991, .T. ) ;
#17505=PLANE ( 'NONE',  #17320 ) ;
#17512=ADVANCED_FACE ( 'NONE', ( #6796 ), #16457, .F. ) ;
#17535=FACE_OUTER_BOUND ( 'NONE', #14990, .T. ) ;
#17640=LINE ( 'NONE', #15846, #13665 ) ;
#17648=CARTESIAN_POINT ( 'NONE',  ( 31.49315201223960159, -2.613324229818170252, -13.00000000000039968 ) ) ;
#17671=ORIENTED_EDGE ( 'NONE', *, *, #5487, .T. ) ;
#17693=ORIENTED_EDGE ( 'NONE', *, *, #10859, .T. ) ;
#17726=ORIENTED_EDGE ( 'NONE', *, *, #22829, .F. ) ;
#17871=DIRECTION ( 'NONE',  ( 0.000000000000000000, 0.000000000000000000, -1.000000000000000000 ) ) ;
#17914=( BOUNDED_CURVE ( )  B_SPLINE_CURVE ( 2, ( #12096, #3039, #10310 ),
 .UNSPECIFIED., .F., .F. ) 
 B_SPLINE_CURVE_WITH_KNOTS ( ( 3, 3 ),
 ( 0.1168436138077924430, 0.2336872276155859962 ),
 .UNSPECIFIED. ) 
 CURVE ( )  GEOMETRIC_REPRESENTATION_ITEM ( )  RATIONAL_B_SPLINE_CURVE ( ( 1.077350269189625065, 1.077350269189625287, 1.000000000000000000 ) ) 
 REPRESENTATION_ITEM ( '' )  );
#17993=CARTESIAN_POINT ( 'NONE',  ( 33.37436288052550282, -3.059220458576433099, -10.50000000000039968 ) ) ;
#17995=VERTEX_POINT ( 'NONE', #6771 ) ;
#18029=CARTESIAN_POINT ( 'NONE',  ( 28.14554285793940025, -3.006546890859610244, -15.00000000000039968 ) ) ;
#18048=CARTESIAN_POINT ( 'NONE',  ( 52.26033179423370001, -7.535689554643980159, -13.00000000000039968 ) ) ;
#18085=DIRECTION ( 'NONE',  ( 1.000000000000000000, 0.000000000000000000, 0.000000000000000000 ) ) ;
#18099=DIRECTION ( 'NONE',  ( 0.000000000000000000, 1.000000000000000000, 0.000000000000000000 ) ) ;
#18100=ORIENTED_EDGE ( 'NONE', *, *, #158, .T. ) ;
#18159=ORIENTED_EDGE ( 'NONE', *, *, #6126, .T. ) ;
#18216=VERTEX_POINT ( 'NONE', #10812 ) ;
#18231=EDGE_CURVE ( 'NONE', #21488, #17995, #19115, .T. ) ;
#18296=DIRECTION ( 'NONE',  ( -0.1997366180463770735, -0.8426774492125654881, -0.4999999999999997780 ) ) ;
#18299=CARTESIAN_POINT ( 'NONE',  ( 33.27705887009690144, -3.036156860537199798, -13.00000000000039968 ) ) ;
#18321=AXIS2_PLACEMENT_3D ( 'NONE', #1292, #13998, #9864 ) ;
#18371=VERTEX_POINT ( 'NONE', #20510 ) ;
#18389=CARTESIAN_POINT ( 'NONE',  ( 33.37436288052550282, -3.059220458576433099, -15.50000000000040146 ) ) ;
#18417=VERTEX_POINT ( 'NONE', #22283 ) ;
#18432=ORIENTED_EDGE ( 'NONE', *, *, #3883, .T. ) ;
#18460=DIRECTION ( 'NONE',  ( -8.623081276789554834E-17, -1.054188326053478339E-16, -1.000000000000000000 ) ) ;
#18478=CARTESIAN_POINT ( 'NONE',  ( 29.36184298829660122, -3.294841866349869974, -11.00000000000039968 ) ) ;
#18488=CIRCLE ( 'NONE', #1016, 3.750000000000000000 ) ;
#18526=DIRECTION ( 'NONE',  ( -0.2306359803922028995, -0.9730401042858036753, 1.343075398093749487E-16 ) ) ;
#18602=CARTESIAN_POINT ( 'NONE',  ( 32.77470933150577537, -5.589124729719509688, -13.00000000000039968 ) ) ;
#18618=ORIENTED_EDGE ( 'NONE', *, *, #3622, .F. ) ;
#18731=AXIS2_PLACEMENT_3D ( 'NONE', #7298, #14541, #21776 ) ;
#18775=CYLINDRICAL_SURFACE ( 'NONE', #13402, 2.500000000000000444 ) ;
#18785=ORIENTED_EDGE ( 'NONE', *, *, #3171, .T. ) ;
#18787=CARTESIAN_POINT ( 'NONE',  ( 33.37436288052550282, -3.059220458576419777, -13.00000000000039968 ) ) ;
#18831=DIRECTION ( 'NONE',  ( -0.9730401042858035643, 0.2306359803922028717, 6.126766849694256332E-17 ) ) ;
#18897=VECTOR ( 'NONE', #21785, 999.9999999999998863 ) ;
#18898=VERTEX_POINT ( 'NONE', #22369 ) ;
#18921=CARTESIAN_POINT ( 'NONE',  ( 31.11077410011089839, -1.335996977273280262, -15.00000000000039968 ) ) ;
#18940=FACE_OUTER_BOUND ( 'NONE', #7265, .T. ) ;
#18963=CARTESIAN_POINT ( 'NONE',  ( 30.31182762792540331, -4.706706774123539994, -13.00000000000039968 ) ) ;
#18977=ORIENTED_EDGE ( 'NONE', *, *, #22294, .T. ) ;
#19115=CIRCLE ( 'NONE', #22892, 2.500000000000000444 ) ;
#19134=VERTEX_POINT ( 'NONE', #17993 ) ;
#19146=CARTESIAN_POINT ( 'NONE',  ( 28.89837840081079889, -1.998294948772289858, -13.00000000000039968 ) ) ;
#19224=AXIS2_PLACEMENT_3D ( 'NONE', #5441, #16469, #20165 ) ;
#19333=CIRCLE ( 'NONE', #15531, 0.09999999999999999167 ) ;
#19359=EDGE_CURVE ( 'NONE', #12704, #14320, #623, .T. ) ;
#19381=EDGE_LOOP ( 'NONE', ( #10757, #13765, #23047, #12839 ) ) ;
#19406=ORIENTED_EDGE ( 'NONE', *, *, #16363, .T. ) ;
#19480=VECTOR ( 'NONE', #8476, 1000.000000000000114 ) ;
#19499=LINE ( 'NONE', #11935, #8070 ) ;
#19562=DIRECTION ( 'NONE',  ( 0.9730401042858035643, -0.2306359803922028717, -5.432877459303547053E-17 ) ) ;
#19628=VECTOR ( 'NONE', #19893, 999.9999999999998863 ) ;
#19676=ORIENTED_EDGE ( 'NONE', *, *, #5694, .F. ) ;
#19696=LINE ( 'NONE', #7233, #22480 ) ;
#19720=EDGE_CURVE ( 'NONE', #13535, #15230, #4263, .T. ) ;
#19806=AXIS2_PLACEMENT_3D ( 'NONE', #4946, #10199, #13859 ) ;
#19830=CIRCLE ( 'NONE', #7693, 4.250000000000000000 ) ;
#19862=CARTESIAN_POINT ( 'NONE',  ( 28.67817383939640052, -0.7594070262927730131, -15.00000000000039968 ) ) ;
#19876=DIRECTION ( 'NONE',  ( 5.798605125234323991E-17, -1.374421231021384554E-17, 1.000000000000000000 ) ) ;
#19893=DIRECTION ( 'NONE',  ( 0.9730401042858036753, -0.2306359803922028995, -5.432877459303547669E-17 ) ) ;
#19895=CARTESIAN_POINT ( 'NONE',  ( 27.54697342219713718, -5.531877349647952080, -13.00000000000039968 ) ) ;
#19967=DIRECTION ( 'NONE',  ( -0.4865200521429013936, 0.1153179901961013387, -0.8660254037844388186 ) ) ;
#20002=AXIS2_PLACEMENT_3D ( 'NONE', #17648, #16309, #17871 ) ;
#20003=ADVANCED_FACE ( 'NONE', ( #21557 ), #1489, .T. ) ;
#20059=PLANE ( 'NONE',  #8792 ) ;
#20070=ADVANCED_FACE ( 'NONE', ( #15875 ), #12558, .T. ) ;
#20140=CLOSED_SHELL ( 'NONE', ( #22248, #17388, #20702, #11191, #20070, #17512, #6891, #8136, #16811, #3106, #2821, #15569, #8788, #20003, #5365, #15215, #3267, #20553, #16652, #21213, #13622 ) ) ;
#20165=DIRECTION ( 'NONE',  ( 0.000000000000000000, -1.000000000000000000, 9.355573283744330345E-16 ) ) ;
#20213=AXIS2_PLACEMENT_3D ( 'NONE', #3559, #14358, #2000 ) ;
#20252=AXIS2_PLACEMENT_3D ( 'NONE', #10431, #6733, #13965 ) ;
#20260=EDGE_LOOP ( 'NONE', ( #4895, #13504, #7698, #14542 ) ) ;
#20262=PLANE ( 'NONE',  #1515 ) ;
#20340=CIRCLE ( 'NONE', #10121, 4.250000000000000000 ) ;
#20344=DIRECTION ( 'NONE',  ( 0.9730401042858036753, -0.2306359803922028995, -5.432877459303547669E-17 ) ) ;
#20371=ORIENTED_EDGE ( 'NONE', *, *, #16368, .F. ) ;
#20429=ORIENTED_EDGE ( 'NONE', *, *, #1837, .F. ) ;
#20476=VECTOR ( 'NONE', #23320, 999.9999999999998863 ) ;
#20480=ORIENTED_EDGE ( 'NONE', *, *, #9799, .F. ) ;
#20510=CARTESIAN_POINT ( 'NONE',  ( 30.57814311865390167, -3.583136841840119935, -15.00000000000039968 ) ) ;
#20523=CARTESIAN_POINT ( 'NONE',  ( 28.27870060330360147, -2.444761924717900214, -11.00000000000039968 ) ) ;
#20533=EDGE_LOOP ( 'NONE', ( #23339, #11322, #5182, #11775, #18618 ) ) ;
#20553=ADVANCED_FACE ( 'NONE', ( #10417 ), #15736, .F. ) ;
#20582=ORIENTED_EDGE ( 'NONE', *, *, #19720, .F. ) ;
#20606=FACE_OUTER_BOUND ( 'NONE', #7592, .T. ) ;
#20686=VERTEX_POINT ( 'NONE', #5386 ) ;
#20695=CARTESIAN_POINT ( 'NONE',  ( 43.98050001724070057, -5.573152644851429471, -10.50000000000039968 ) ) ;
#20702=ADVANCED_FACE ( 'NONE', ( #11108 ), #16806, .T. ) ;
#20710=CARTESIAN_POINT ( 'NONE',  ( 33.37436288052550282, -3.059220458576419777, -13.00000000000039968 ) ) ;
#20720=VERTEX_POINT ( 'NONE', #379 ) ;
#20737=VERTEX_POINT ( 'NONE', #9191 ) ;
#20757=CIRCLE ( 'NONE', #10542, 4.250000000000000000 ) ;
#20760=AXIS2_PLACEMENT_3D ( 'NONE', #7423, #21886, #4081 ) ;
#20832=ORIENTED_EDGE ( 'NONE', *, *, #6330, .T. ) ;
#20835=CARTESIAN_POINT ( 'NONE',  ( 33.37436288052550282, -3.059220458576419777, -13.00000000000039968 ) ) ;
#20936=AXIS2_PLACEMENT_3D ( 'NONE', #1376, #3180, #8645 ) ;
#21001=EDGE_CURVE ( 'NONE', #13190, #18417, #510, .T. ) ;
#21014=ORIENTED_EDGE ( 'NONE', *, *, #310, .F. ) ;
#21032=DIRECTION ( 'NONE',  ( 0.000000000000000000, 1.020425574104004122E-16, 1.000000000000000000 ) ) ;
#21064=CARTESIAN_POINT ( 'NONE',  ( 30.57814311865390167, -3.583136841840119935, -11.00000000000039968 ) ) ;
#21090=EDGE_LOOP ( 'NONE', ( #22653, #22754, #7279, #3342, #16286 ) ) ;
#21154=DIRECTION ( 'NONE',  ( -0.1153179901961009640, -0.4865200521429018377, 0.8660254037844385966 ) ) ;
#21179=DIRECTION ( 'NONE',  ( 0.000000000000000000, 0.000000000000000000, -1.000000000000000000 ) ) ;
#21213=ADVANCED_FACE ( 'NONE', ( #16401 ), #1905, .F. ) ;
#21302=VERTEX_POINT ( 'NONE', #21619 ) ;
#21342=ORIENTED_EDGE ( 'NONE', *, *, #5470, .F. ) ;
#21399=CARTESIAN_POINT ( 'NONE',  ( 33.27705887009690144, -3.036156860537199798, -13.00000000000039968 ) ) ;
#21453=ORIENTED_EDGE ( 'NONE', *, *, #6070, .F. ) ;
#21488=VERTEX_POINT ( 'NONE', #18389 ) ;
#21557=FACE_OUTER_BOUND ( 'NONE', #21090, .T. ) ;
#21580=DIRECTION ( 'NONE',  ( 0.9730401042858036753, -0.2306359803922028995, -5.432877459303547669E-17 ) ) ;
#21587=FACE_OUTER_BOUND ( 'NONE', #7224, .T. ) ;
#21619=CARTESIAN_POINT ( 'NONE',  ( 30.57814311865390167, -3.583136841840119935, -11.00000000000039968 ) ) ;
#21659=EDGE_CURVE ( 'NONE', #2641, #18216, #20340, .T. ) ;
#21683=EDGE_LOOP ( 'NONE', ( #8453, #18159, #665, #7230, #22312 ) ) ;
#21737=CARTESIAN_POINT ( 'NONE',  ( 27.87922736721089834, -4.130116823143030302, -13.00000000000039968 ) ) ;
#21775=VERTEX_POINT ( 'NONE', #11520 ) ;
#21776=DIRECTION ( 'NONE',  ( -0.2306359803922028995, -0.9730401042858035643, -1.064172857958375654E-32 ) ) ;
#21785=DIRECTION ( 'NONE',  ( -0.9730401042858036753, 0.2306359803922028995, 5.959266323858677443E-17 ) ) ;
#21815=PLANE ( 'NONE',  #19224 ) ;
#21879=ORIENTED_EDGE ( 'NONE', *, *, #21659, .T. ) ;
#21886=DIRECTION ( 'NONE',  ( 0.9730401042858035643, -0.2306359803922028717, -5.959266323858667582E-17 ) ) ;
#22061=AXIS2_PLACEMENT_3D ( 'NONE', #3709, #5257, #12519 ) ;
#22069=VECTOR ( 'NONE', #3588, 999.9999999999998863 ) ;
#22145=ORIENTED_EDGE ( 'NONE', *, *, #3883, .F. ) ;
#22239=AXIS2_PLACEMENT_3D ( 'NONE', #22656, #13527, #4499 ) ;
#22248=ADVANCED_FACE ( 'NONE', ( #8861 ), #16202, .F. ) ;
#22283=CARTESIAN_POINT ( 'NONE',  ( 52.26033179423370001, -7.535689554643993482, -10.50000000000039968 ) ) ;
#22294=EDGE_CURVE ( 'NONE', #5571, #23086, #16201, .T. ) ;
#22312=ORIENTED_EDGE ( 'NONE', *, *, #13991, .F. ) ;
#22347=CARTESIAN_POINT ( 'NONE',  ( 31.56827854690370927, -0.8510906712623030890, -14.00000000000040146 ) ) ;
#22369=CARTESIAN_POINT ( 'NONE',  ( 28.67817383939640052, -0.7594070262927701265, -11.00000000000039968 ) ) ;
#22458=LINE ( 'NONE', #7622, #13925 ) ;
#22480=VECTOR ( 'NONE', #12466, 1000.000000000000114 ) ;
#22520=ORIENTED_EDGE ( 'NONE', *, *, #8208, .F. ) ;
#22532=EDGE_CURVE ( 'NONE', #15230, #13535, #8264, .T. ) ;
#22543=FACE_OUTER_BOUND ( 'NONE', #19381, .T. ) ;
#22608=LINE ( 'NONE', #11842, #20476 ) ;
#22653=ORIENTED_EDGE ( 'NONE', *, *, #22294, .F. ) ;
#22656=CARTESIAN_POINT ( 'NONE',  ( 52.49909637502329929, -7.592283011512620305, -13.00000000000039968 ) ) ;
#22754=ORIENTED_EDGE ( 'NONE', *, *, #16840, .F. ) ;
#22829=EDGE_CURVE ( 'NONE', #15338, #7111, #16372, .T. ) ;
#22833=VECTOR ( 'NONE', #1836, 999.9999999999998863 ) ;
#22852=DIRECTION ( 'NONE',  ( 0.1997366180463766849, 0.8426774492125652660, -0.5000000000000004441 ) ) ;
#22892=AXIS2_PLACEMENT_3D ( 'NONE', #20835, #14468, #12699 ) ;
#23003=CONICAL_SURFACE ( 'NONE', #22239, 2.254620000000000513, 0.7853981633974461696 ) ;
#23014=ORIENTED_EDGE ( 'NONE', *, *, #5053, .T. ) ;
#23047=ORIENTED_EDGE ( 'NONE', *, *, #21001, .T. ) ;
#23085=FACE_BOUND ( 'NONE', #1435, .T. ) ;
#23086=VERTEX_POINT ( 'NONE', #9628 ) ;
#23113=EDGE_CURVE ( 'NONE', #18898, #20737, #2483, .T. ) ;
#23117=CARTESIAN_POINT ( 'NONE',  ( 28.07896398525720016, -3.287439373930470143, -14.50000000000040146 ) ) ;
#23201=CIRCLE ( 'NONE', #19806, 2.500000000000000444 ) ;
#23320=DIRECTION ( 'NONE',  ( -0.9730401042858036753, 0.2306359803922028995, 5.959266323858677443E-17 ) ) ;
#23339=ORIENTED_EDGE ( 'NONE', *, *, #6126, .F. ) ;
#23349=AXIS2_PLACEMENT_3D ( 'NONE', #18048, #3625, #7315 ) ;
#23449=EDGE_LOOP ( 'NONE', ( #21453, #2342, #17430, #16770 ) ) ;
#23471=DIRECTION ( 'NONE',  ( 0.000000000000000000, 1.020425574104004122E-16, 1.000000000000000000 ) ) ;
#23529=COLOUR_RGB('Sky Blue', 0.31764706, 0.68627451, 0.89019608);
#23530=FILL_AREA_STYLE_COLOUR('',#23529);
#23531=FILL_AREA_STYLE('',(#23530));
#23532=SURFACE_STYLE_FILL_AREA(#23531);
#23533=SURFACE_SIDE_STYLE('',(#23532));
#23534=SURFACE_STYLE_USAGE(.BOTH.,#23533);
#23535=PRESENTATION_STYLE_ASSIGNMENT((#23534));
#23593=STYLED_ITEM('',(#23535),#1311);
#23594=MECHANICAL_DESIGN_GEOMETRIC_PRESENTATION_REPRESENTATION('',(#23593),#11790);
ENDSEC;
END-ISO-10303-21;
